ISO-10303-21;
HEADER;
/* Generated by software containing ST-Developer
 * from STEP Tools, Inc. (www.steptools.com) 
 */

FILE_DESCRIPTION(
/* description */ ('Crank-driven oscillating fan base (mechanism only)'),

/* implementation_level */ '2;1');

FILE_NAME(
/* name */ 'Link pin (1).step',
/* time_stamp */ '2026-10-28T03:25:00-07:00',
/* author */ (''),
/* organization */ (''),
/* preprocessor_version */ 'ST-DEVELOPER v20.2',
/* originating_system */ 'Autodesk Translation Framework v15.17.0.0',
/* authorisation */ '');

FILE_SCHEMA (('AUTOMOTIVE_DESIGN { 1 0 10303 214 3 1 1 }'));
ENDSEC;

DATA;
#10=MECHANICAL_DESIGN_GEOMETRIC_PRESENTATION_REPRESENTATION('',(#474),#11916);
#386=SHAPE_REPRESENTATION_RELATIONSHIP('SRR','None',#12113,#426);
#426=ADVANCED_BREP_SHAPE_REPRESENTATION('',(#521),#11904);
#474=STYLED_ITEM('',(#12375),#521);
#521=MANIFOLD_SOLID_BREP('Body1',#6105);
#669=FACE_BOUND('',#1693,.T.);
#670=FACE_BOUND('',#1695,.T.);
#671=FACE_BOUND('',#1700,.T.);
#672=FACE_BOUND('',#1702,.T.);
#833=PLANE('',#7195);
#834=PLANE('',#7199);
#835=PLANE('',#7200);
#836=PLANE('',#7203);
#837=PLANE('',#7211);
#838=PLANE('',#7212);
#1174=FACE_OUTER_BOUND('',#1688,.T.);
#1175=FACE_OUTER_BOUND('',#1689,.T.);
#1176=FACE_OUTER_BOUND('',#1690,.T.);
#1177=FACE_OUTER_BOUND('',#1691,.T.);
#1178=FACE_OUTER_BOUND('',#1692,.T.);
#1179=FACE_OUTER_BOUND('',#1694,.T.);
#1180=FACE_OUTER_BOUND('',#1696,.T.);
#1181=FACE_OUTER_BOUND('',#1697,.T.);
#1182=FACE_OUTER_BOUND('',#1698,.T.);
#1183=FACE_OUTER_BOUND('',#1699,.T.);
#1184=FACE_OUTER_BOUND('',#1701,.T.);
#1688=EDGE_LOOP('',(#5238,#5239,#5240,#5241));
#1689=EDGE_LOOP('',(#5242));
#1690=EDGE_LOOP('',(#5243,#5244,#5245,#5246));
#1691=EDGE_LOOP('',(#5247));
#1692=EDGE_LOOP('',(#5248));
#1693=EDGE_LOOP('',(#5249));
#1694=EDGE_LOOP('',(#5250));
#1695=EDGE_LOOP('',(#5251));
#1696=EDGE_LOOP('',(#5252,#5253,#5254,#5255));
#1697=EDGE_LOOP('',(#5256,#5257,#5258,#5259));
#1698=EDGE_LOOP('',(#5260,#5261,#5262,#5263));
#1699=EDGE_LOOP('',(#5264));
#1700=EDGE_LOOP('',(#5265));
#1701=EDGE_LOOP('',(#5266));
#1702=EDGE_LOOP('',(#5267));
#2037=LINE('',#11414,#2370);
#2038=LINE('',#11421,#2371);
#2039=LINE('',#11435,#2372);
#2040=LINE('',#11438,#2373);
#2041=LINE('',#11443,#2374);
#2370=VECTOR('',#8920,0.164999999999999);
#2371=VECTOR('',#8929,0.164999999999999);
#2372=VECTOR('',#8948,0.699999999999999);
#2373=VECTOR('',#8951,0.300000000000001);
#2374=VECTOR('',#8958,0.300000000000001);
#2769=CIRCLE('',#7193,0.164999999999999);
#2770=CIRCLE('',#7194,0.164999999999999);
#2771=CIRCLE('',#7197,0.164999999999999);
#2772=CIRCLE('',#7198,0.164999999999999);
#2773=CIRCLE('',#7201,0.699999999999999);
#2774=CIRCLE('',#7202,0.300000000000001);
#2775=CIRCLE('',#7204,0.699999999999999);
#2776=CIRCLE('',#7205,0.300000000000001);
#2777=CIRCLE('',#7208,0.300000000000001);
#2778=CIRCLE('',#7210,0.300000000000001);
#3229=VERTEX_POINT('',#11411);
#3230=VERTEX_POINT('',#11413);
#3231=VERTEX_POINT('',#11418);
#3232=VERTEX_POINT('',#11420);
#3233=VERTEX_POINT('',#11425);
#3234=VERTEX_POINT('',#11427);
#3235=VERTEX_POINT('',#11430);
#3236=VERTEX_POINT('',#11432);
#3237=VERTEX_POINT('',#11437);
#3238=VERTEX_POINT('',#11441);
#3914=EDGE_CURVE('',#3229,#3229,#2769,.T.);
#3915=EDGE_CURVE('',#3229,#3230,#2037,.T.);
#3916=EDGE_CURVE('',#3230,#3230,#2770,.T.);
#3917=EDGE_CURVE('',#3231,#3231,#2771,.T.);
#3918=EDGE_CURVE('',#3231,#3232,#2038,.T.);
#3919=EDGE_CURVE('',#3232,#3232,#2772,.T.);
#3920=EDGE_CURVE('',#3233,#3233,#2773,.T.);
#3921=EDGE_CURVE('',#3234,#3234,#2774,.T.);
#3922=EDGE_CURVE('',#3235,#3235,#2775,.T.);
#3923=EDGE_CURVE('',#3236,#3236,#2776,.T.);
#3924=EDGE_CURVE('',#3233,#3235,#2039,.T.);
#3925=EDGE_CURVE('',#3236,#3237,#2040,.T.);
#3926=EDGE_CURVE('',#3237,#3237,#2777,.T.);
#3927=EDGE_CURVE('',#3238,#3238,#2778,.T.);
#3928=EDGE_CURVE('',#3238,#3234,#2041,.T.);
#5238=ORIENTED_EDGE('',*,*,#3914,.F.);
#5239=ORIENTED_EDGE('',*,*,#3915,.T.);
#5240=ORIENTED_EDGE('',*,*,#3916,.F.);
#5241=ORIENTED_EDGE('',*,*,#3915,.F.);
#5242=ORIENTED_EDGE('',*,*,#3914,.T.);
#5243=ORIENTED_EDGE('',*,*,#3917,.F.);
#5244=ORIENTED_EDGE('',*,*,#3918,.T.);
#5245=ORIENTED_EDGE('',*,*,#3919,.T.);
#5246=ORIENTED_EDGE('',*,*,#3918,.F.);
#5247=ORIENTED_EDGE('',*,*,#3919,.F.);
#5248=ORIENTED_EDGE('',*,*,#3920,.T.);
#5249=ORIENTED_EDGE('',*,*,#3921,.F.);
#5250=ORIENTED_EDGE('',*,*,#3922,.F.);
#5251=ORIENTED_EDGE('',*,*,#3923,.F.);
#5252=ORIENTED_EDGE('',*,*,#3920,.F.);
#5253=ORIENTED_EDGE('',*,*,#3924,.T.);
#5254=ORIENTED_EDGE('',*,*,#3922,.T.);
#5255=ORIENTED_EDGE('',*,*,#3924,.F.);
#5256=ORIENTED_EDGE('',*,*,#3923,.T.);
#5257=ORIENTED_EDGE('',*,*,#3925,.T.);
#5258=ORIENTED_EDGE('',*,*,#3926,.T.);
#5259=ORIENTED_EDGE('',*,*,#3925,.F.);
#5260=ORIENTED_EDGE('',*,*,#3927,.F.);
#5261=ORIENTED_EDGE('',*,*,#3928,.T.);
#5262=ORIENTED_EDGE('',*,*,#3921,.T.);
#5263=ORIENTED_EDGE('',*,*,#3928,.F.);
#5264=ORIENTED_EDGE('',*,*,#3927,.T.);
#5265=ORIENTED_EDGE('',*,*,#3916,.T.);
#5266=ORIENTED_EDGE('',*,*,#3926,.F.);
#5267=ORIENTED_EDGE('',*,*,#3917,.T.);
#5666=CYLINDRICAL_SURFACE('',#7192,0.164999999999999);
#5667=CYLINDRICAL_SURFACE('',#7196,0.164999999999999);
#5668=CYLINDRICAL_SURFACE('',#7206,0.699999999999999);
#5669=CYLINDRICAL_SURFACE('',#7207,0.300000000000001);
#5670=CYLINDRICAL_SURFACE('',#7209,0.300000000000001);
#5980=ADVANCED_FACE('',(#1174),#5666,.F.);
#5981=ADVANCED_FACE('',(#1175),#833,.T.);
#5982=ADVANCED_FACE('',(#1176),#5667,.F.);
#5983=ADVANCED_FACE('',(#1177),#834,.F.);
#5984=ADVANCED_FACE('',(#1178,#669),#835,.T.);
#5985=ADVANCED_FACE('',(#1179,#670),#836,.F.);
#5986=ADVANCED_FACE('',(#1180),#5668,.T.);
#5987=ADVANCED_FACE('',(#1181),#5669,.T.);
#5988=ADVANCED_FACE('',(#1182),#5670,.T.);
#5989=ADVANCED_FACE('',(#1183,#671),#837,.T.);
#5990=ADVANCED_FACE('',(#1184,#672),#838,.F.);
#6105=CLOSED_SHELL('',(#5980,#5981,#5982,#5983,#5984,#5985,#5986,#5987,
#5988,#5989,#5990));
#7191=AXIS2_PLACEMENT_3D('',#11409,#8914,#8915);
#7192=AXIS2_PLACEMENT_3D('',#11410,#8916,#8917);
#7193=AXIS2_PLACEMENT_3D('',#11412,#8918,#8919);
#7194=AXIS2_PLACEMENT_3D('',#11415,#8921,#8922);
#7195=AXIS2_PLACEMENT_3D('',#11416,#8923,#8924);
#7196=AXIS2_PLACEMENT_3D('',#11417,#8925,#8926);
#7197=AXIS2_PLACEMENT_3D('',#11419,#8927,#8928);
#7198=AXIS2_PLACEMENT_3D('',#11422,#8930,#8931);
#7199=AXIS2_PLACEMENT_3D('',#11423,#8932,#8933);
#7200=AXIS2_PLACEMENT_3D('',#11424,#8934,#8935);
#7201=AXIS2_PLACEMENT_3D('',#11426,#8936,#8937);
#7202=AXIS2_PLACEMENT_3D('',#11428,#8938,#8939);
#7203=AXIS2_PLACEMENT_3D('',#11429,#8940,#8941);
#7204=AXIS2_PLACEMENT_3D('',#11431,#8942,#8943);
#7205=AXIS2_PLACEMENT_3D('',#11433,#8944,#8945);
#7206=AXIS2_PLACEMENT_3D('',#11434,#8946,#8947);
#7207=AXIS2_PLACEMENT_3D('',#11436,#8949,#8950);
#7208=AXIS2_PLACEMENT_3D('',#11439,#8952,#8953);
#7209=AXIS2_PLACEMENT_3D('',#11440,#8954,#8955);
#7210=AXIS2_PLACEMENT_3D('',#11442,#8956,#8957);
#7211=AXIS2_PLACEMENT_3D('',#11444,#8959,#8960);
#7212=AXIS2_PLACEMENT_3D('',#11445,#8961,#8962);
#8914=DIRECTION('axis',(0.,0.,1.));
#8915=DIRECTION('refdir',(1.,0.,0.));
#8916=DIRECTION('center_axis',(0.,0.,1.));
#8917=DIRECTION('ref_axis',(1.,0.,0.));
#8918=DIRECTION('center_axis',(0.,0.,1.));
#8919=DIRECTION('ref_axis',(1.,0.,0.));
#8920=DIRECTION('',(0.,0.,1.));
#8921=DIRECTION('center_axis',(0.,0.,-1.));
#8922=DIRECTION('ref_axis',(1.,0.,0.));
#8923=DIRECTION('center_axis',(0.,0.,1.));
#8924=DIRECTION('ref_axis',(1.,0.,0.));
#8925=DIRECTION('center_axis',(0.,0.,1.));
#8926=DIRECTION('ref_axis',(1.,0.,0.));
#8927=DIRECTION('center_axis',(0.,0.,1.));
#8928=DIRECTION('ref_axis',(1.,0.,0.));
#8929=DIRECTION('',(0.,0.,1.));
#8930=DIRECTION('center_axis',(0.,0.,1.));
#8931=DIRECTION('ref_axis',(1.,0.,0.));
#8932=DIRECTION('center_axis',(0.,0.,1.));
#8933=DIRECTION('ref_axis',(1.,0.,0.));
#8934=DIRECTION('center_axis',(0.,0.,1.));
#8935=DIRECTION('ref_axis',(1.,0.,0.));
#8936=DIRECTION('center_axis',(0.,0.,1.));
#8937=DIRECTION('ref_axis',(1.,0.,0.));
#8938=DIRECTION('center_axis',(0.,0.,1.));
#8939=DIRECTION('ref_axis',(1.,0.,0.));
#8940=DIRECTION('center_axis',(0.,0.,1.));
#8941=DIRECTION('ref_axis',(1.,0.,0.));
#8942=DIRECTION('center_axis',(0.,0.,1.));
#8943=DIRECTION('ref_axis',(1.,0.,0.));
#8944=DIRECTION('center_axis',(0.,0.,-1.));
#8945=DIRECTION('ref_axis',(1.,0.,0.));
#8946=DIRECTION('center_axis',(0.,0.,1.));
#8947=DIRECTION('ref_axis',(1.,0.,0.));
#8948=DIRECTION('',(0.,0.,-1.));
#8949=DIRECTION('center_axis',(0.,0.,1.));
#8950=DIRECTION('ref_axis',(1.,0.,0.));
#8951=DIRECTION('',(0.,0.,-1.));
#8952=DIRECTION('center_axis',(0.,0.,1.));
#8953=DIRECTION('ref_axis',(1.,0.,0.));
#8954=DIRECTION('center_axis',(0.,0.,1.));
#8955=DIRECTION('ref_axis',(1.,0.,0.));
#8956=DIRECTION('center_axis',(0.,0.,1.));
#8957=DIRECTION('ref_axis',(1.,0.,0.));
#8958=DIRECTION('',(0.,0.,-1.));
#8959=DIRECTION('center_axis',(0.,0.,1.));
#8960=DIRECTION('ref_axis',(1.,0.,0.));
#8961=DIRECTION('center_axis',(0.,0.,1.));
#8962=DIRECTION('ref_axis',(1.,0.,0.));
#11409=CARTESIAN_POINT('',(0.,0.,0.));
#11410=CARTESIAN_POINT('Origin',(8.,4.,8.7));
#11411=CARTESIAN_POINT('',(7.835,4.,8.7));
#11412=CARTESIAN_POINT('Origin',(8.,4.,8.7));
#11413=CARTESIAN_POINT('',(7.835,4.,9.6));
#11414=CARTESIAN_POINT('',(7.835,4.,8.7));
#11415=CARTESIAN_POINT('Origin',(8.,4.,9.6));
#11416=CARTESIAN_POINT('Origin',(8.,4.,8.7));
#11417=CARTESIAN_POINT('Origin',(8.,4.,6.1));
#11418=CARTESIAN_POINT('',(7.835,4.,6.2));
#11419=CARTESIAN_POINT('Origin',(8.,4.,6.2));
#11420=CARTESIAN_POINT('',(7.835,4.,7.8));
#11421=CARTESIAN_POINT('',(7.835,4.,6.1));
#11422=CARTESIAN_POINT('Origin',(8.,4.,7.8));
#11423=CARTESIAN_POINT('Origin',(8.,4.,7.8));
#11424=CARTESIAN_POINT('Origin',(8.,4.,7.4));
#11425=CARTESIAN_POINT('',(7.3,4.,7.4));
#11426=CARTESIAN_POINT('Origin',(8.,4.,7.4));
#11427=CARTESIAN_POINT('',(7.7,4.,7.4));
#11428=CARTESIAN_POINT('Origin',(8.,4.,7.4));
#11429=CARTESIAN_POINT('Origin',(8.,4.,7.));
#11430=CARTESIAN_POINT('',(7.3,4.,7.));
#11431=CARTESIAN_POINT('Origin',(8.,4.,7.));
#11432=CARTESIAN_POINT('',(7.7,4.,7.));
#11433=CARTESIAN_POINT('Origin',(8.,4.,7.));
#11434=CARTESIAN_POINT('Origin',(8.,4.,7.));
#11435=CARTESIAN_POINT('',(7.3,4.,7.));
#11436=CARTESIAN_POINT('Origin',(8.,4.,6.2));
#11437=CARTESIAN_POINT('',(7.7,4.,6.2));
#11438=CARTESIAN_POINT('',(7.7,4.,6.2));
#11439=CARTESIAN_POINT('Origin',(8.,4.,6.2));
#11440=CARTESIAN_POINT('Origin',(8.,4.,6.2));
#11441=CARTESIAN_POINT('',(7.7,4.,9.6));
#11442=CARTESIAN_POINT('Origin',(8.,4.,9.6));
#11443=CARTESIAN_POINT('',(7.7,4.,6.2));
#11444=CARTESIAN_POINT('Origin',(8.,4.,9.6));
#11445=CARTESIAN_POINT('Origin',(8.,4.,6.2));
#11857=UNCERTAINTY_MEASURE_WITH_UNIT(LENGTH_MEASURE(0.001),#11917,
'DISTANCE_ACCURACY_VALUE',
'Maximum model space distance between geometric entities at asserted c
onnectivities');
#11869=UNCERTAINTY_MEASURE_WITH_UNIT(LENGTH_MEASURE(0.001),#11917,
'DISTANCE_ACCURACY_VALUE',
'Maximum model space distance between geometric entities at asserted c
onnectivities');
#11904=(
GEOMETRIC_REPRESENTATION_CONTEXT(3)
GLOBAL_UNCERTAINTY_ASSIGNED_CONTEXT((#11857))
GLOBAL_UNIT_ASSIGNED_CONTEXT((#11917,#11919,#11920))
REPRESENTATION_CONTEXT('','3D')
);
#11916=(
GEOMETRIC_REPRESENTATION_CONTEXT(3)
GLOBAL_UNCERTAINTY_ASSIGNED_CONTEXT((#11869))
GLOBAL_UNIT_ASSIGNED_CONTEXT((#11917,#11919,#11920))
REPRESENTATION_CONTEXT('','3D')
);
#11917=(
LENGTH_UNIT()
NAMED_UNIT(*)
SI_UNIT(.CENTI.,.METRE.)
);
#11919=(
NAMED_UNIT(*)
PLANE_ANGLE_UNIT()
SI_UNIT($,.RADIAN.)
);
#11920=(
NAMED_UNIT(*)
SI_UNIT($,.STERADIAN.)
SOLID_ANGLE_UNIT()
);
#11955=SHAPE_DEFINITION_REPRESENTATION(#12006,#12113);
#12006=PRODUCT_DEFINITION_SHAPE('',$,#12160);
#12113=SHAPE_REPRESENTATION('',(#7191),#11904);
#12125=PRODUCT_DEFINITION_CONTEXT('part definition',#12265,'design');
#12160=PRODUCT_DEFINITION('Link pin (1)','Link pin (1)',#12206,#12125);
#12206=PRODUCT_DEFINITION_FORMATION('',$,#12301);
#12265=APPLICATION_CONTEXT(
'Core Data for Automotive Mechanical Design Process');
#12266=PRODUCT_CONTEXT('part definition',#12265,'mechanical');
#12301=PRODUCT('Link pin (1)','Link pin (1)','Link pin (1)',(#12266));
#12369=COLOUR_RGB('Grey',0.48,0.52,0.57);
#12370=FILL_AREA_STYLE_COLOUR('',#12369);
#12371=FILL_AREA_STYLE('',(#12370));
#12372=SURFACE_STYLE_FILL_AREA(#12371);
#12373=SURFACE_SIDE_STYLE('',(#12372));
#12374=SURFACE_STYLE_USAGE(.BOTH.,#12373);
#12375=PRESENTATION_STYLE_ASSIGNMENT((#12374));
ENDSEC;
END-ISO-10303-21;
